ISO-10303-21;
HEADER;
/* Generated by software containing ST-Developer
 * from STEP Tools, Inc. (www.steptools.com) 
 */

FILE_DESCRIPTION(
/* description */ ('Fatigue rig crank-slider'),
/* implementation_level */ '2;1');

FILE_NAME(
/* name */ 'Flat Washer - M8.step',
/* time_stamp */ '2026-10-28T03:24:50-07:00',
/* author */ (''),
/* organization */ (''),
/* preprocessor_version */ 'ST-DEVELOPER v20.2',
/* originating_system */ 'Autodesk Translation Framework v15.17.0.0',
/* authorisation */ '');

FILE_SCHEMA (('AUTOMOTIVE_DESIGN { 1 0 10303 214 3 1 1 }'));
ENDSEC;

DATA;
#10=MECHANICAL_DESIGN_GEOMETRIC_PRESENTATION_REPRESENTATION('',(#600),#16911);
#499=SHAPE_REPRESENTATION_RELATIONSHIP('SRR','None',#17139,#549);
#549=ADVANCED_BREP_SHAPE_REPRESENTATION('',(#659),#16868);
#600=STYLED_ITEM('',(#17494),#659);
#659=MANIFOLD_SOLID_BREP('Body1',#8891);
#805=FACE_BOUND('',#2005,.T.);
#806=FACE_BOUND('',#2007,.T.);
#985=PLANE('',#9804);
#986=PLANE('',#9805);
#1374=FACE_OUTER_BOUND('',#2002,.T.);
#1375=FACE_OUTER_BOUND('',#2003,.T.);
#1376=FACE_OUTER_BOUND('',#2004,.T.);
#1377=FACE_OUTER_BOUND('',#2006,.T.);
#2002=EDGE_LOOP('',(#6664,#6665,#6666,#6667));
#2003=EDGE_LOOP('',(#6668,#6669,#6670,#6671));
#2004=EDGE_LOOP('',(#6672));
#2005=EDGE_LOOP('',(#6673));
#2006=EDGE_LOOP('',(#6674));
#2007=EDGE_LOOP('',(#6675));
#2640=LINE('',#14509,#3286);
#2641=LINE('',#14515,#3287);
#3286=VECTOR('',#11360,0.42);
#3287=VECTOR('',#11367,0.8);
#3882=CIRCLE('',#9799,0.42);
#3883=CIRCLE('',#9800,0.42);
#3884=CIRCLE('',#9802,0.8);
#3885=CIRCLE('',#9803,0.8);
#4382=VERTEX_POINT('',#14506);
#4383=VERTEX_POINT('',#14508);
#4384=VERTEX_POINT('',#14512);
#4385=VERTEX_POINT('',#14514);
#5230=EDGE_CURVE('',#4382,#4382,#3882,.T.);
#5231=EDGE_CURVE('',#4382,#4383,#2640,.T.);
#5232=EDGE_CURVE('',#4383,#4383,#3883,.T.);
#5233=EDGE_CURVE('',#4384,#4384,#3884,.T.);
#5234=EDGE_CURVE('',#4384,#4385,#2641,.T.);
#5235=EDGE_CURVE('',#4385,#4385,#3885,.T.);
#6664=ORIENTED_EDGE('',*,*,#5230,.F.);
#6665=ORIENTED_EDGE('',*,*,#5231,.T.);
#6666=ORIENTED_EDGE('',*,*,#5232,.T.);
#6667=ORIENTED_EDGE('',*,*,#5231,.F.);
#6668=ORIENTED_EDGE('',*,*,#5233,.F.);
#6669=ORIENTED_EDGE('',*,*,#5234,.T.);
#6670=ORIENTED_EDGE('',*,*,#5235,.T.);
#6671=ORIENTED_EDGE('',*,*,#5234,.F.);
#6672=ORIENTED_EDGE('',*,*,#5233,.T.);
#6673=ORIENTED_EDGE('',*,*,#5230,.T.);
#6674=ORIENTED_EDGE('',*,*,#5235,.F.);
#6675=ORIENTED_EDGE('',*,*,#5232,.F.);
#8263=CYLINDRICAL_SURFACE('',#9798,0.42);
#8264=CYLINDRICAL_SURFACE('',#9801,0.8);
#8512=ADVANCED_FACE('',(#1374),#8263,.F.);
#8513=ADVANCED_FACE('',(#1375),#8264,.T.);
#8514=ADVANCED_FACE('',(#1376,#805),#985,.T.);
#8515=ADVANCED_FACE('',(#1377,#806),#986,.F.);
#8891=CLOSED_SHELL('',(#8512,#8513,#8514,#8515));
#9797=AXIS2_PLACEMENT_3D('',#14504,#11354,#11355);
#9798=AXIS2_PLACEMENT_3D('',#14505,#11356,#11357);
#9799=AXIS2_PLACEMENT_3D('',#14507,#11358,#11359);
#9800=AXIS2_PLACEMENT_3D('',#14510,#11361,#11362);
#9801=AXIS2_PLACEMENT_3D('',#14511,#11363,#11364);
#9802=AXIS2_PLACEMENT_3D('',#14513,#11365,#11366);
#9803=AXIS2_PLACEMENT_3D('',#14516,#11368,#11369);
#9804=AXIS2_PLACEMENT_3D('',#14517,#11370,#11371);
#9805=AXIS2_PLACEMENT_3D('',#14518,#11372,#11373);
#11354=DIRECTION('axis',(0.,0.,1.));
#11355=DIRECTION('refdir',(1.,0.,0.));
#11356=DIRECTION('center_axis',(0.,1.,0.));
#11357=DIRECTION('ref_axis',(1.,0.,0.));
#11358=DIRECTION('center_axis',(0.,-1.,0.));
#11359=DIRECTION('ref_axis',(1.,0.,0.));
#11360=DIRECTION('',(0.,-1.,0.));
#11361=DIRECTION('center_axis',(0.,-1.,0.));
#11362=DIRECTION('ref_axis',(1.,0.,0.));
#11363=DIRECTION('center_axis',(0.,1.,0.));
#11364=DIRECTION('ref_axis',(1.,0.,0.));
#11365=DIRECTION('center_axis',(0.,1.,0.));
#11366=DIRECTION('ref_axis',(1.,0.,0.));
#11367=DIRECTION('',(0.,-1.,0.));
#11368=DIRECTION('center_axis',(0.,1.,0.));
#11369=DIRECTION('ref_axis',(1.,0.,0.));
#11370=DIRECTION('center_axis',(0.,1.,0.));
#11371=DIRECTION('ref_axis',(1.,0.,0.));
#11372=DIRECTION('center_axis',(0.,1.,0.));
#11373=DIRECTION('ref_axis',(1.,0.,0.));
#14504=CARTESIAN_POINT('',(0.,0.,0.));
#14505=CARTESIAN_POINT('Origin',(0.,0.,0.));
#14506=CARTESIAN_POINT('',(-0.42,0.16,5.14351655641888E-17));
#14507=CARTESIAN_POINT('Origin',(0.,0.16,0.));
#14508=CARTESIAN_POINT('',(-0.42,0.,5.14351655641888E-17));
#14509=CARTESIAN_POINT('',(-0.42,0.,5.14351655641888E-17));
#14510=CARTESIAN_POINT('Origin',(0.,0.,0.));
#14511=CARTESIAN_POINT('Origin',(0.,0.,0.));
#14512=CARTESIAN_POINT('',(-0.8,0.16,9.79717439317883E-17));
#14513=CARTESIAN_POINT('Origin',(0.,0.16,0.));
#14514=CARTESIAN_POINT('',(-0.8,0.,9.79717439317883E-17));
#14515=CARTESIAN_POINT('',(-0.8,0.,9.79717439317883E-17));
#14516=CARTESIAN_POINT('Origin',(0.,0.,0.));
#14517=CARTESIAN_POINT('Origin',(0.,0.16,0.));
#14518=CARTESIAN_POINT('Origin',(0.,0.,0.));
#16809=UNCERTAINTY_MEASURE_WITH_UNIT(LENGTH_MEASURE(0.001),#16912,
'DISTANCE_ACCURACY_VALUE',
'Maximum model space distance between geometric entities at asserted c
onnectivities');
#16852=UNCERTAINTY_MEASURE_WITH_UNIT(LENGTH_MEASURE(0.001),#16912,
'DISTANCE_ACCURACY_VALUE',
'Maximum model space distance between geometric entities at asserted c
onnectivities');
#16868=(
GEOMETRIC_REPRESENTATION_CONTEXT(3)
GLOBAL_UNCERTAINTY_ASSIGNED_CONTEXT((#16809))
GLOBAL_UNIT_ASSIGNED_CONTEXT((#16912,#16914,#16915))
REPRESENTATION_CONTEXT('','3D')
);
#16911=(
GEOMETRIC_REPRESENTATION_CONTEXT(3)
GLOBAL_UNCERTAINTY_ASSIGNED_CONTEXT((#16852))
GLOBAL_UNIT_ASSIGNED_CONTEXT((#16912,#16914,#16915))
REPRESENTATION_CONTEXT('','3D')
);
#16912=(
LENGTH_UNIT()
NAMED_UNIT(*)
SI_UNIT(.CENTI.,.METRE.)
);
#16914=(
NAMED_UNIT(*)
PLANE_ANGLE_UNIT()
SI_UNIT($,.RADIAN.)
);
#16915=(
NAMED_UNIT(*)
SI_UNIT($,.STERADIAN.)
SOLID_ANGLE_UNIT()
);
#16931=SHAPE_DEFINITION_REPRESENTATION(#16991,#17139);
#16991=PRODUCT_DEFINITION_SHAPE('',$,#17198);
#17139=SHAPE_REPRESENTATION('',(#9797),#16868);
#17182=PRODUCT_DEFINITION_CONTEXT('part definition',#17358,'design');
#17198=PRODUCT_DEFINITION('Flat Washer - M8','Flat Washer - M8',#17256,
#17182);
#17256=PRODUCT_DEFINITION_FORMATION('',$,#17375);
#17358=APPLICATION_CONTEXT(
'Core Data for Automotive Mechanical Design Process');
#17359=PRODUCT_CONTEXT('part definition',#17358,'mechanical');
#17375=PRODUCT('Flat Washer - M8','Flat Washer - M8','Flat Washer - M8',
(#17359));
#17488=COLOUR_RGB('Black',0.12,0.14,0.17);
#17489=FILL_AREA_STYLE_COLOUR('',#17488);
#17490=FILL_AREA_STYLE('',(#17489));
#17491=SURFACE_STYLE_FILL_AREA(#17490);
#17492=SURFACE_SIDE_STYLE('',(#17491));
#17493=SURFACE_STYLE_USAGE(.BOTH.,#17492);
#17494=PRESENTATION_STYLE_ASSIGNMENT((#17493));
ENDSEC;
END-ISO-10303-21;
